ISO-10303-21;
HEADER;
/* Generated by software containing ST-Developer
 * from STEP Tools, Inc. (www.steptools.com) 
 */

FILE_DESCRIPTION(
/* description */ ('Drill jig with bushing plate'),
/* implementation_level */ '2;1');

FILE_NAME(
/* name */ 'Drill bushing 8 (1).step',
/* time_stamp */ '2026-10-27T10:51:08-07:00',
/* author */ (''),
/* organization */ (''),
/* preprocessor_version */ 'ST-DEVELOPER v20.2',
/* originating_system */ 'Autodesk Translation Framework v15.17.0.0',
/* authorisation */ '');

FILE_SCHEMA (('AUTOMOTIVE_DESIGN { 1 0 10303 214 3 1 1 }'));
ENDSEC;

DATA;
#10=MECHANICAL_DESIGN_GEOMETRIC_PRESENTATION_REPRESENTATION('',(#242),#6638);
#194=SHAPE_REPRESENTATION_RELATIONSHIP('SRR','None',#6759,#218);
#218=ADVANCED_BREP_SHAPE_REPRESENTATION('',(#264),#6632);
#242=STYLED_ITEM('',(#6957),#264);
#264=MANIFOLD_SOLID_BREP('Body1',#3611);
#358=FACE_BOUND('',#989,.T.);
#359=FACE_BOUND('',#992,.T.);
#360=FACE_BOUND('',#996,.T.);
#484=PLANE('',#4258);
#485=PLANE('',#4263);
#486=PLANE('',#4269);
#685=FACE_OUTER_BOUND('',#988,.T.);
#686=FACE_OUTER_BOUND('',#990,.T.);
#687=FACE_OUTER_BOUND('',#991,.T.);
#688=FACE_OUTER_BOUND('',#993,.T.);
#689=FACE_OUTER_BOUND('',#994,.T.);
#690=FACE_OUTER_BOUND('',#995,.T.);
#988=EDGE_LOOP('',(#3203));
#989=EDGE_LOOP('',(#3204));
#990=EDGE_LOOP('',(#3205,#3206,#3207,#3208));
#991=EDGE_LOOP('',(#3209));
#992=EDGE_LOOP('',(#3210));
#993=EDGE_LOOP('',(#3211,#3212,#3213,#3214));
#994=EDGE_LOOP('',(#3215,#3216,#3217,#3218));
#995=EDGE_LOOP('',(#3219));
#996=EDGE_LOOP('',(#3220));
#1269=LINE('',#6464,#1530);
#1270=LINE('',#6470,#1531);
#1271=LINE('',#6474,#1532);
#1530=VECTOR('',#5332,0.8);
#1531=VECTOR('',#5339,0.4);
#1532=VECTOR('',#5344,0.6);
#1694=CIRCLE('',#4259,0.8);
#1695=CIRCLE('',#4260,0.6);
#1696=CIRCLE('',#4262,0.8);
#1697=CIRCLE('',#4264,0.4);
#1698=CIRCLE('',#4266,0.4);
#1699=CIRCLE('',#4268,0.6);
#1974=VERTEX_POINT('',#6457);
#1975=VERTEX_POINT('',#6459);
#1976=VERTEX_POINT('',#6462);
#1977=VERTEX_POINT('',#6466);
#1978=VERTEX_POINT('',#6469);
#1979=VERTEX_POINT('',#6473);
#2389=EDGE_CURVE('',#1974,#1974,#1694,.T.);
#2390=EDGE_CURVE('',#1975,#1975,#1695,.T.);
#2391=EDGE_CURVE('',#1976,#1976,#1696,.T.);
#2392=EDGE_CURVE('',#1976,#1974,#1269,.T.);
#2393=EDGE_CURVE('',#1977,#1977,#1697,.T.);
#2394=EDGE_CURVE('',#1977,#1978,#1270,.T.);
#2395=EDGE_CURVE('',#1978,#1978,#1698,.T.);
#2396=EDGE_CURVE('',#1975,#1979,#1271,.T.);
#2397=EDGE_CURVE('',#1979,#1979,#1699,.T.);
#3203=ORIENTED_EDGE('',*,*,#2389,.F.);
#3204=ORIENTED_EDGE('',*,*,#2390,.T.);
#3205=ORIENTED_EDGE('',*,*,#2391,.F.);
#3206=ORIENTED_EDGE('',*,*,#2392,.T.);
#3207=ORIENTED_EDGE('',*,*,#2389,.T.);
#3208=ORIENTED_EDGE('',*,*,#2392,.F.);
#3209=ORIENTED_EDGE('',*,*,#2391,.T.);
#3210=ORIENTED_EDGE('',*,*,#2393,.T.);
#3211=ORIENTED_EDGE('',*,*,#2393,.F.);
#3212=ORIENTED_EDGE('',*,*,#2394,.T.);
#3213=ORIENTED_EDGE('',*,*,#2395,.T.);
#3214=ORIENTED_EDGE('',*,*,#2394,.F.);
#3215=ORIENTED_EDGE('',*,*,#2390,.F.);
#3216=ORIENTED_EDGE('',*,*,#2396,.T.);
#3217=ORIENTED_EDGE('',*,*,#2397,.T.);
#3218=ORIENTED_EDGE('',*,*,#2396,.F.);
#3219=ORIENTED_EDGE('',*,*,#2397,.F.);
#3220=ORIENTED_EDGE('',*,*,#2395,.F.);
#3363=CYLINDRICAL_SURFACE('',#4261,0.8);
#3364=CYLINDRICAL_SURFACE('',#4265,0.4);
#3365=CYLINDRICAL_SURFACE('',#4267,0.6);
#3560=ADVANCED_FACE('',(#685,#358),#484,.F.);
#3561=ADVANCED_FACE('',(#686),#3363,.T.);
#3562=ADVANCED_FACE('',(#687,#359),#485,.T.);
#3563=ADVANCED_FACE('',(#688),#3364,.F.);
#3564=ADVANCED_FACE('',(#689),#3365,.T.);
#3565=ADVANCED_FACE('',(#690,#360),#486,.F.);
#3611=CLOSED_SHELL('',(#3560,#3561,#3562,#3563,#3564,#3565));
#4257=AXIS2_PLACEMENT_3D('',#6455,#5320,#5321);
#4258=AXIS2_PLACEMENT_3D('',#6456,#5322,#5323);
#4259=AXIS2_PLACEMENT_3D('',#6458,#5324,#5325);
#4260=AXIS2_PLACEMENT_3D('',#6460,#5326,#5327);
#4261=AXIS2_PLACEMENT_3D('',#6461,#5328,#5329);
#4262=AXIS2_PLACEMENT_3D('',#6463,#5330,#5331);
#4263=AXIS2_PLACEMENT_3D('',#6465,#5333,#5334);
#4264=AXIS2_PLACEMENT_3D('',#6467,#5335,#5336);
#4265=AXIS2_PLACEMENT_3D('',#6468,#5337,#5338);
#4266=AXIS2_PLACEMENT_3D('',#6471,#5340,#5341);
#4267=AXIS2_PLACEMENT_3D('',#6472,#5342,#5343);
#4268=AXIS2_PLACEMENT_3D('',#6475,#5345,#5346);
#4269=AXIS2_PLACEMENT_3D('',#6476,#5347,#5348);
#5320=DIRECTION('axis',(0.,0.,1.));
#5321=DIRECTION('refdir',(1.,0.,0.));
#5322=DIRECTION('center_axis',(0.,0.,1.));
#5323=DIRECTION('ref_axis',(1.,0.,0.));
#5324=DIRECTION('center_axis',(0.,0.,1.));
#5325=DIRECTION('ref_axis',(1.,0.,0.));
#5326=DIRECTION('center_axis',(0.,0.,1.));
#5327=DIRECTION('ref_axis',(1.,0.,0.));
#5328=DIRECTION('center_axis',(0.,0.,1.));
#5329=DIRECTION('ref_axis',(1.,0.,0.));
#5330=DIRECTION('center_axis',(0.,0.,1.));
#5331=DIRECTION('ref_axis',(1.,0.,0.));
#5332=DIRECTION('',(0.,0.,-1.));
#5333=DIRECTION('center_axis',(0.,0.,1.));
#5334=DIRECTION('ref_axis',(1.,0.,0.));
#5335=DIRECTION('center_axis',(0.,0.,-1.));
#5336=DIRECTION('ref_axis',(1.,0.,0.));
#5337=DIRECTION('center_axis',(0.,0.,1.));
#5338=DIRECTION('ref_axis',(1.,0.,0.));
#5339=DIRECTION('',(0.,0.,-1.));
#5340=DIRECTION('center_axis',(0.,0.,-1.));
#5341=DIRECTION('ref_axis',(1.,0.,0.));
#5342=DIRECTION('center_axis',(0.,0.,1.));
#5343=DIRECTION('ref_axis',(1.,0.,0.));
#5344=DIRECTION('',(0.,0.,-1.));
#5345=DIRECTION('center_axis',(0.,0.,1.));
#5346=DIRECTION('ref_axis',(1.,0.,0.));
#5347=DIRECTION('center_axis',(0.,0.,1.));
#5348=DIRECTION('ref_axis',(1.,0.,0.));
#6455=CARTESIAN_POINT('',(0.,0.,0.));
#6456=CARTESIAN_POINT('Origin',(-2.,1.,4.5));
#6457=CARTESIAN_POINT('',(-2.8,1.,4.5));
#6458=CARTESIAN_POINT('Origin',(-2.,1.,4.5));
#6459=CARTESIAN_POINT('',(-2.6,1.,4.5));
#6460=CARTESIAN_POINT('Origin',(-2.,1.,4.5));
#6461=CARTESIAN_POINT('Origin',(-2.,1.,4.5));
#6462=CARTESIAN_POINT('',(-2.8,1.,4.7));
#6463=CARTESIAN_POINT('Origin',(-2.,1.,4.7));
#6464=CARTESIAN_POINT('',(-2.8,1.,4.5));
#6465=CARTESIAN_POINT('Origin',(-2.,1.,4.7));
#6466=CARTESIAN_POINT('',(-2.4,1.,4.7));
#6467=CARTESIAN_POINT('Origin',(-2.,1.,4.7));
#6468=CARTESIAN_POINT('Origin',(-2.,1.,2.5));
#6469=CARTESIAN_POINT('',(-2.4,1.,2.5));
#6470=CARTESIAN_POINT('',(-2.4,1.,2.5));
#6471=CARTESIAN_POINT('Origin',(-2.,1.,2.5));
#6472=CARTESIAN_POINT('Origin',(-2.,1.,2.5));
#6473=CARTESIAN_POINT('',(-2.6,1.,2.5));
#6474=CARTESIAN_POINT('',(-2.6,1.,2.5));
#6475=CARTESIAN_POINT('Origin',(-2.,1.,2.5));
#6476=CARTESIAN_POINT('Origin',(-2.,1.,2.5));
#6603=UNCERTAINTY_MEASURE_WITH_UNIT(LENGTH_MEASURE(0.001),#6639,
'DISTANCE_ACCURACY_VALUE',
'Maximum model space distance between geometric entities at asserted c
onnectivities');
#6609=UNCERTAINTY_MEASURE_WITH_UNIT(LENGTH_MEASURE(0.001),#6639,
'DISTANCE_ACCURACY_VALUE',
'Maximum model space distance between geometric entities at asserted c
onnectivities');
#6632=(
GEOMETRIC_REPRESENTATION_CONTEXT(3)
GLOBAL_UNCERTAINTY_ASSIGNED_CONTEXT((#6603))
GLOBAL_UNIT_ASSIGNED_CONTEXT((#6639,#6641,#6642))
REPRESENTATION_CONTEXT('','3D')
);
#6638=(
GEOMETRIC_REPRESENTATION_CONTEXT(3)
GLOBAL_UNCERTAINTY_ASSIGNED_CONTEXT((#6609))
GLOBAL_UNIT_ASSIGNED_CONTEXT((#6639,#6641,#6642))
REPRESENTATION_CONTEXT('','3D')
);
#6639=(
LENGTH_UNIT()
NAMED_UNIT(*)
SI_UNIT(.CENTI.,.METRE.)
);
#6641=(
NAMED_UNIT(*)
PLANE_ANGLE_UNIT()
SI_UNIT($,.RADIAN.)
);
#6642=(
NAMED_UNIT(*)
SI_UNIT($,.STERADIAN.)
SOLID_ANGLE_UNIT()
);
#6665=SHAPE_DEFINITION_REPRESENTATION(#6721,#6759);
#6721=PRODUCT_DEFINITION_SHAPE('',$,#6788);
#6759=SHAPE_REPRESENTATION('',(#4257),#6632);
#6765=PRODUCT_DEFINITION_CONTEXT('part definition',#6851,'design');
#6788=PRODUCT_DEFINITION('Drill bushing 8 (1)','Drill bushing 8 (1)',#6816,
#6765);
#6816=PRODUCT_DEFINITION_FORMATION('',$,#6875);
#6851=APPLICATION_CONTEXT(
'Core Data for Automotive Mechanical Design Process');
#6852=PRODUCT_CONTEXT('part definition',#6851,'mechanical');
#6875=PRODUCT('Drill bushing 8 (1)','Drill bushing 8 (1)',
'Drill bushing 8 (1)',(#6852));
#6951=COLOUR_RGB('Off White',0.89,0.88,0.83);
#6952=FILL_AREA_STYLE_COLOUR('',#6951);
#6953=FILL_AREA_STYLE('',(#6952));
#6954=SURFACE_STYLE_FILL_AREA(#6953);
#6955=SURFACE_SIDE_STYLE('',(#6954));
#6956=SURFACE_STYLE_USAGE(.BOTH.,#6955);
#6957=PRESENTATION_STYLE_ASSIGNMENT((#6956));
ENDSEC;
END-ISO-10303-21;
